ISO-10303-21;
HEADER;
/* Generated by software containing ST-Developer
 * from STEP Tools, Inc. (www.steptools.com) 
 */

FILE_DESCRIPTION(
/* description */ ('Located fixture plate with toggle clamp'),
/* implementation_level */ '2;1');

FILE_NAME(
/* name */ 'Hex Bolt - M6 x 30 mm.step',
/* time_stamp */ '2026-10-27T21:36:12-07:00',
/* author */ (''),
/* organization */ (''),
/* preprocessor_version */ 'ST-DEVELOPER v20.2',
/* originating_system */ 'Autodesk Translation Framework v15.17.0.0',
/* authorisation */ '');

FILE_SCHEMA (('AUTOMOTIVE_DESIGN { 1 0 10303 214 3 1 1 }'));
ENDSEC;

DATA;
#10=MECHANICAL_DESIGN_GEOMETRIC_PRESENTATION_REPRESENTATION('',(#327),#9285);
#204=(
BOUNDED_CURVE()
B_SPLINE_CURVE(2,(#8213,#8214,#8215),.UNSPECIFIED.,.F.,.F.)
B_SPLINE_CURVE_WITH_KNOTS((3,3),(0.144988513094728,0.791574906712449),
 .UNSPECIFIED.)
CURVE()
GEOMETRIC_REPRESENTATION_ITEM()
RATIONAL_B_SPLINE_CURVE((1.09282032302755,1.26188021535082,1.09282032302931))
REPRESENTATION_ITEM('')
);
#205=(
BOUNDED_CURVE()
B_SPLINE_CURVE(2,(#8217,#8218,#8219),.UNSPECIFIED.,.F.,.F.)
B_SPLINE_CURVE_WITH_KNOTS((3,3),(0.144988513094728,0.791574906712449),
 .UNSPECIFIED.)
CURVE()
GEOMETRIC_REPRESENTATION_ITEM()
RATIONAL_B_SPLINE_CURVE((1.09282032302755,1.26188021535082,1.09282032302931))
REPRESENTATION_ITEM('')
);
#206=(
BOUNDED_CURVE()
B_SPLINE_CURVE(2,(#8221,#8222,#8223),.UNSPECIFIED.,.F.,.F.)
B_SPLINE_CURVE_WITH_KNOTS((3,3),(0.144988513094728,0.791574906712449),
 .UNSPECIFIED.)
CURVE()
GEOMETRIC_REPRESENTATION_ITEM()
RATIONAL_B_SPLINE_CURVE((1.09282032302755,1.26188021535082,1.09282032302931))
REPRESENTATION_ITEM('')
);
#207=(
BOUNDED_CURVE()
B_SPLINE_CURVE(2,(#8225,#8226,#8227),.UNSPECIFIED.,.F.,.F.)
B_SPLINE_CURVE_WITH_KNOTS((3,3),(0.144988513094728,0.791574906712449),
 .UNSPECIFIED.)
CURVE()
GEOMETRIC_REPRESENTATION_ITEM()
RATIONAL_B_SPLINE_CURVE((1.09282032302755,1.26188021535082,1.09282032302931))
REPRESENTATION_ITEM('')
);
#208=(
BOUNDED_CURVE()
B_SPLINE_CURVE(2,(#8229,#8230,#8231),.UNSPECIFIED.,.F.,.F.)
B_SPLINE_CURVE_WITH_KNOTS((3,3),(0.144988513094728,0.791574906712449),
 .UNSPECIFIED.)
CURVE()
GEOMETRIC_REPRESENTATION_ITEM()
RATIONAL_B_SPLINE_CURVE((1.09282032302755,1.26188021535082,1.09282032302931))
REPRESENTATION_ITEM('')
);
#209=(
BOUNDED_CURVE()
B_SPLINE_CURVE(2,(#8232,#8233,#8234),.UNSPECIFIED.,.F.,.F.)
B_SPLINE_CURVE_WITH_KNOTS((3,3),(0.144988513094727,0.791574906712449),
 .UNSPECIFIED.)
CURVE()
GEOMETRIC_REPRESENTATION_ITEM()
RATIONAL_B_SPLINE_CURVE((1.09282032302755,1.26188021535082,1.09282032302931))
REPRESENTATION_ITEM('')
);
#254=CONICAL_SURFACE('',#5689,0.27,0.785398163397448);
#255=CONICAL_SURFACE('',#5692,0.576175134594813,1.0471975511966);
#279=SHAPE_REPRESENTATION_RELATIONSHIP('SRR','None',#9402,#303);
#303=ADVANCED_BREP_SHAPE_REPRESENTATION('',(#350),#9264);
#327=STYLED_ITEM('',(#9619),#350);
#350=MANIFOLD_SOLID_BREP('Body1',#5176);
#448=FACE_BOUND('',#1182,.T.);
#557=PLANE('',#5691);
#558=PLANE('',#5694);
#559=PLANE('',#5695);
#560=PLANE('',#5696);
#561=PLANE('',#5697);
#562=PLANE('',#5698);
#563=PLANE('',#5699);
#564=PLANE('',#5700);
#565=PLANE('',#5701);
#793=FACE_OUTER_BOUND('',#1170,.T.);
#794=FACE_OUTER_BOUND('',#1171,.T.);
#795=FACE_OUTER_BOUND('',#1172,.T.);
#796=FACE_OUTER_BOUND('',#1173,.T.);
#797=FACE_OUTER_BOUND('',#1174,.T.);
#798=FACE_OUTER_BOUND('',#1175,.T.);
#799=FACE_OUTER_BOUND('',#1176,.T.);
#800=FACE_OUTER_BOUND('',#1177,.T.);
#801=FACE_OUTER_BOUND('',#1178,.T.);
#802=FACE_OUTER_BOUND('',#1179,.T.);
#803=FACE_OUTER_BOUND('',#1180,.T.);
#804=FACE_OUTER_BOUND('',#1181,.T.);
#1170=EDGE_LOOP('',(#4076,#4077,#4078,#4079));
#1171=EDGE_LOOP('',(#4080,#4081,#4082,#4083));
#1172=EDGE_LOOP('',(#4084));
#1173=EDGE_LOOP('',(#4085,#4086,#4087,#4088,#4089,#4090,#4091,#4092,#4093));
#1174=EDGE_LOOP('',(#4094,#4095,#4096,#4097));
#1175=EDGE_LOOP('',(#4098,#4099,#4100,#4101));
#1176=EDGE_LOOP('',(#4102,#4103,#4104,#4105));
#1177=EDGE_LOOP('',(#4106,#4107,#4108,#4109));
#1178=EDGE_LOOP('',(#4110,#4111,#4112,#4113));
#1179=EDGE_LOOP('',(#4114,#4115,#4116,#4117));
#1180=EDGE_LOOP('',(#4118));
#1181=EDGE_LOOP('',(#4119,#4120,#4121,#4122,#4123,#4124));
#1182=EDGE_LOOP('',(#4125));
#1479=CIRCLE('',#5687,0.2942);
#1480=CIRCLE('',#5688,0.2942);
#1481=CIRCLE('',#5690,0.24);
#1482=CIRCLE('',#5693,0.475);
#1781=LINE('',#8200,#2191);
#1782=LINE('',#8205,#2192);
#1783=LINE('',#8211,#2193);
#1784=LINE('',#8237,#2194);
#1785=LINE('',#8239,#2195);
#1786=LINE('',#8240,#2196);
#1787=LINE('',#8243,#2197);
#1788=LINE('',#8244,#2198);
#1789=LINE('',#8247,#2199);
#1790=LINE('',#8248,#2200);
#1791=LINE('',#8251,#2201);
#1792=LINE('',#8252,#2202);
#1793=LINE('',#8255,#2203);
#1794=LINE('',#8256,#2204);
#1795=LINE('',#8258,#2205);
#2191=VECTOR('',#6683,0.3);
#2192=VECTOR('',#6690,0.27);
#2193=VECTOR('',#6697,0.576175134594813);
#2194=VECTOR('',#6700,1.);
#2195=VECTOR('',#6701,1.);
#2196=VECTOR('',#6702,1.);
#2197=VECTOR('',#6705,1.);
#2198=VECTOR('',#6706,1.);
#2199=VECTOR('',#6709,1.);
#2200=VECTOR('',#6710,1.);
#2201=VECTOR('',#6713,1.);
#2202=VECTOR('',#6714,1.);
#2203=VECTOR('',#6717,1.);
#2204=VECTOR('',#6718,1.);
#2205=VECTOR('',#6721,1.);
#2597=VERTEX_POINT('',#8197);
#2598=VERTEX_POINT('',#8199);
#2599=VERTEX_POINT('',#8203);
#2600=VERTEX_POINT('',#8208);
#2601=VERTEX_POINT('',#8210);
#2602=VERTEX_POINT('',#8212);
#2603=VERTEX_POINT('',#8216);
#2604=VERTEX_POINT('',#8220);
#2605=VERTEX_POINT('',#8224);
#2606=VERTEX_POINT('',#8228);
#2607=VERTEX_POINT('',#8236);
#2608=VERTEX_POINT('',#8238);
#2609=VERTEX_POINT('',#8242);
#2610=VERTEX_POINT('',#8246);
#2611=VERTEX_POINT('',#8250);
#2612=VERTEX_POINT('',#8254);
#3126=EDGE_CURVE('',#2597,#2597,#1479,.F.);
#3127=EDGE_CURVE('',#2597,#2598,#1781,.T.);
#3128=EDGE_CURVE('',#2598,#2598,#1480,.F.);
#3129=EDGE_CURVE('',#2599,#2599,#1481,.T.);
#3130=EDGE_CURVE('',#2599,#2597,#1782,.T.);
#3131=EDGE_CURVE('',#2600,#2600,#1482,.T.);
#3132=EDGE_CURVE('',#2600,#2601,#1783,.T.);
#3133=EDGE_CURVE('',#2602,#2601,#204,.T.);
#3134=EDGE_CURVE('',#2603,#2602,#205,.T.);
#3135=EDGE_CURVE('',#2604,#2603,#206,.T.);
#3136=EDGE_CURVE('',#2605,#2604,#207,.T.);
#3137=EDGE_CURVE('',#2606,#2605,#208,.T.);
#3138=EDGE_CURVE('',#2601,#2606,#209,.T.);
#3139=EDGE_CURVE('',#2607,#2605,#1784,.T.);
#3140=EDGE_CURVE('',#2607,#2608,#1785,.T.);
#3141=EDGE_CURVE('',#2608,#2606,#1786,.T.);
#3142=EDGE_CURVE('',#2609,#2604,#1787,.T.);
#3143=EDGE_CURVE('',#2609,#2607,#1788,.T.);
#3144=EDGE_CURVE('',#2610,#2603,#1789,.T.);
#3145=EDGE_CURVE('',#2610,#2609,#1790,.T.);
#3146=EDGE_CURVE('',#2611,#2602,#1791,.T.);
#3147=EDGE_CURVE('',#2611,#2610,#1792,.T.);
#3148=EDGE_CURVE('',#2612,#2601,#1793,.T.);
#3149=EDGE_CURVE('',#2612,#2611,#1794,.T.);
#3150=EDGE_CURVE('',#2608,#2612,#1795,.T.);
#4076=ORIENTED_EDGE('',*,*,#3126,.F.);
#4077=ORIENTED_EDGE('',*,*,#3127,.T.);
#4078=ORIENTED_EDGE('',*,*,#3128,.F.);
#4079=ORIENTED_EDGE('',*,*,#3127,.F.);
#4080=ORIENTED_EDGE('',*,*,#3129,.F.);
#4081=ORIENTED_EDGE('',*,*,#3130,.T.);
#4082=ORIENTED_EDGE('',*,*,#3126,.T.);
#4083=ORIENTED_EDGE('',*,*,#3130,.F.);
#4084=ORIENTED_EDGE('',*,*,#3129,.T.);
#4085=ORIENTED_EDGE('',*,*,#3131,.F.);
#4086=ORIENTED_EDGE('',*,*,#3132,.T.);
#4087=ORIENTED_EDGE('',*,*,#3133,.F.);
#4088=ORIENTED_EDGE('',*,*,#3134,.F.);
#4089=ORIENTED_EDGE('',*,*,#3135,.F.);
#4090=ORIENTED_EDGE('',*,*,#3136,.F.);
#4091=ORIENTED_EDGE('',*,*,#3137,.F.);
#4092=ORIENTED_EDGE('',*,*,#3138,.F.);
#4093=ORIENTED_EDGE('',*,*,#3132,.F.);
#4094=ORIENTED_EDGE('',*,*,#3137,.T.);
#4095=ORIENTED_EDGE('',*,*,#3139,.F.);
#4096=ORIENTED_EDGE('',*,*,#3140,.T.);
#4097=ORIENTED_EDGE('',*,*,#3141,.T.);
#4098=ORIENTED_EDGE('',*,*,#3136,.T.);
#4099=ORIENTED_EDGE('',*,*,#3142,.F.);
#4100=ORIENTED_EDGE('',*,*,#3143,.T.);
#4101=ORIENTED_EDGE('',*,*,#3139,.T.);
#4102=ORIENTED_EDGE('',*,*,#3135,.T.);
#4103=ORIENTED_EDGE('',*,*,#3144,.F.);
#4104=ORIENTED_EDGE('',*,*,#3145,.T.);
#4105=ORIENTED_EDGE('',*,*,#3142,.T.);
#4106=ORIENTED_EDGE('',*,*,#3134,.T.);
#4107=ORIENTED_EDGE('',*,*,#3146,.F.);
#4108=ORIENTED_EDGE('',*,*,#3147,.T.);
#4109=ORIENTED_EDGE('',*,*,#3144,.T.);
#4110=ORIENTED_EDGE('',*,*,#3133,.T.);
#4111=ORIENTED_EDGE('',*,*,#3148,.F.);
#4112=ORIENTED_EDGE('',*,*,#3149,.T.);
#4113=ORIENTED_EDGE('',*,*,#3146,.T.);
#4114=ORIENTED_EDGE('',*,*,#3138,.T.);
#4115=ORIENTED_EDGE('',*,*,#3141,.F.);
#4116=ORIENTED_EDGE('',*,*,#3150,.T.);
#4117=ORIENTED_EDGE('',*,*,#3148,.T.);
#4118=ORIENTED_EDGE('',*,*,#3131,.T.);
#4119=ORIENTED_EDGE('',*,*,#3145,.F.);
#4120=ORIENTED_EDGE('',*,*,#3147,.F.);
#4121=ORIENTED_EDGE('',*,*,#3149,.F.);
#4122=ORIENTED_EDGE('',*,*,#3150,.F.);
#4123=ORIENTED_EDGE('',*,*,#3140,.F.);
#4124=ORIENTED_EDGE('',*,*,#3143,.F.);
#4125=ORIENTED_EDGE('',*,*,#3128,.T.);
#4837=CYLINDRICAL_SURFACE('',#5686,0.2942);
#4994=ADVANCED_FACE('',(#793),#4837,.T.);
#4995=ADVANCED_FACE('',(#794),#254,.T.);
#4996=ADVANCED_FACE('',(#795),#557,.T.);
#4997=ADVANCED_FACE('',(#796),#255,.T.);
#4998=ADVANCED_FACE('',(#797),#558,.T.);
#4999=ADVANCED_FACE('',(#798),#559,.T.);
#5000=ADVANCED_FACE('',(#799),#560,.T.);
#5001=ADVANCED_FACE('',(#800),#561,.T.);
#5002=ADVANCED_FACE('',(#801),#562,.T.);
#5003=ADVANCED_FACE('',(#802),#563,.T.);
#5004=ADVANCED_FACE('',(#803),#564,.T.);
#5005=ADVANCED_FACE('',(#804,#448),#565,.F.);
#5176=CLOSED_SHELL('',(#4994,#4995,#4996,#4997,#4998,#4999,#5000,#5001,
#5002,#5003,#5004,#5005));
#5685=AXIS2_PLACEMENT_3D('',#8195,#6677,#6678);
#5686=AXIS2_PLACEMENT_3D('',#8196,#6679,#6680);
#5687=AXIS2_PLACEMENT_3D('',#8198,#6681,#6682);
#5688=AXIS2_PLACEMENT_3D('',#8201,#6684,#6685);
#5689=AXIS2_PLACEMENT_3D('',#8202,#6686,#6687);
#5690=AXIS2_PLACEMENT_3D('',#8204,#6688,#6689);
#5691=AXIS2_PLACEMENT_3D('',#8206,#6691,#6692);
#5692=AXIS2_PLACEMENT_3D('',#8207,#6693,#6694);
#5693=AXIS2_PLACEMENT_3D('',#8209,#6695,#6696);
#5694=AXIS2_PLACEMENT_3D('',#8235,#6698,#6699);
#5695=AXIS2_PLACEMENT_3D('',#8241,#6703,#6704);
#5696=AXIS2_PLACEMENT_3D('',#8245,#6707,#6708);
#5697=AXIS2_PLACEMENT_3D('',#8249,#6711,#6712);
#5698=AXIS2_PLACEMENT_3D('',#8253,#6715,#6716);
#5699=AXIS2_PLACEMENT_3D('',#8257,#6719,#6720);
#5700=AXIS2_PLACEMENT_3D('',#8259,#6722,#6723);
#5701=AXIS2_PLACEMENT_3D('',#8260,#6724,#6725);
#6677=DIRECTION('axis',(0.,0.,1.));
#6678=DIRECTION('refdir',(1.,0.,0.));
#6679=DIRECTION('center_axis',(0.,-1.,0.));
#6680=DIRECTION('ref_axis',(1.,0.,0.));
#6681=DIRECTION('center_axis',(0.,1.,0.));
#6682=DIRECTION('ref_axis',(1.,0.,0.));
#6683=DIRECTION('',(0.,1.,0.));
#6684=DIRECTION('center_axis',(0.,-1.,0.));
#6685=DIRECTION('ref_axis',(1.,0.,0.));
#6686=DIRECTION('center_axis',(0.,1.,0.));
#6687=DIRECTION('ref_axis',(1.,0.,0.));
#6688=DIRECTION('center_axis',(0.,-1.,0.));
#6689=DIRECTION('ref_axis',(1.,0.,0.));
#6690=DIRECTION('',(-0.707106781186547,0.707106781186548,-8.65956056235493E-17));
#6691=DIRECTION('center_axis',(0.,-1.,0.));
#6692=DIRECTION('ref_axis',(0.,0.,-1.));
#6693=DIRECTION('center_axis',(0.,-1.,0.));
#6694=DIRECTION('ref_axis',(1.,0.,0.));
#6695=DIRECTION('center_axis',(0.,1.,0.));
#6696=DIRECTION('ref_axis',(1.,0.,0.));
#6697=DIRECTION('',(-0.866025403784439,-0.5,-1.06057523872491E-16));
#6698=DIRECTION('center_axis',(1.92296268638356E-16,0.,-1.));
#6699=DIRECTION('ref_axis',(-1.,0.,-1.92296268638356E-16));
#6700=DIRECTION('',(0.,1.,0.));
#6701=DIRECTION('',(-1.,0.,-1.92296268638356E-16));
#6702=DIRECTION('',(0.,1.,0.));
#6703=DIRECTION('center_axis',(0.866025403784439,0.,-0.5));
#6704=DIRECTION('ref_axis',(-0.5,0.,-0.866025403784439));
#6705=DIRECTION('',(0.,1.,0.));
#6706=DIRECTION('',(-0.5,0.,-0.866025403784439));
#6707=DIRECTION('center_axis',(0.866025403784439,0.,0.5));
#6708=DIRECTION('ref_axis',(0.5,0.,-0.866025403784439));
#6709=DIRECTION('',(0.,1.,0.));
#6710=DIRECTION('',(0.5,0.,-0.866025403784439));
#6711=DIRECTION('center_axis',(-1.92296268638356E-16,0.,1.));
#6712=DIRECTION('ref_axis',(1.,0.,1.92296268638356E-16));
#6713=DIRECTION('',(0.,1.,0.));
#6714=DIRECTION('',(1.,0.,1.92296268638356E-16));
#6715=DIRECTION('center_axis',(-0.866025403784439,0.,0.5));
#6716=DIRECTION('ref_axis',(0.5,0.,0.866025403784439));
#6717=DIRECTION('',(0.,1.,0.));
#6718=DIRECTION('',(0.5,0.,0.866025403784439));
#6719=DIRECTION('center_axis',(-0.866025403784439,0.,-0.5));
#6720=DIRECTION('ref_axis',(-0.5,0.,0.866025403784439));
#6721=DIRECTION('',(-0.5,0.,0.866025403784438));
#6722=DIRECTION('center_axis',(0.,1.,0.));
#6723=DIRECTION('ref_axis',(0.,0.,1.));
#6724=DIRECTION('center_axis',(0.,1.,0.));
#6725=DIRECTION('ref_axis',(1.,0.,0.));
#8195=CARTESIAN_POINT('',(0.,0.,0.));
#8196=CARTESIAN_POINT('Origin',(0.,-1.445,0.));
#8197=CARTESIAN_POINT('',(-0.2942,-2.9458,3.60291088309151E-17));
#8198=CARTESIAN_POINT('Origin',(0.,-2.9458,0.));
#8199=CARTESIAN_POINT('',(-0.2942,0.,-3.60291088309151E-17));
#8200=CARTESIAN_POINT('',(-0.2942,-1.445,-3.60291088309151E-17));
#8201=CARTESIAN_POINT('Origin',(0.,0.,0.));
#8202=CARTESIAN_POINT('Origin',(0.,-2.97,0.));
#8203=CARTESIAN_POINT('',(-0.24,-3.,-2.93915231795365E-17));
#8204=CARTESIAN_POINT('Origin',(0.,-3.,0.));
#8205=CARTESIAN_POINT('',(-0.27,-2.97,-3.30654635769785E-17));
#8206=CARTESIAN_POINT('Origin',(0.,-3.,0.));
#8207=CARTESIAN_POINT('Origin',(0.,0.341586508806388,0.));
#8208=CARTESIAN_POINT('',(-0.475,0.4,-5.81707229594993E-17));
#8209=CARTESIAN_POINT('Origin',(0.,0.4,0.));
#8210=CARTESIAN_POINT('',(-0.577350269189626,0.340908044531739,-7.07050159149938E-17));
#8211=CARTESIAN_POINT('',(-0.576175134594813,0.341586508806388,-7.05611034329833E-17));
#8212=CARTESIAN_POINT('',(-0.288675134594813,0.340908044531739,0.5));
#8213=CARTESIAN_POINT('Ctrl Pts',(-0.288675134594813,0.340908044531739,
0.5));
#8214=CARTESIAN_POINT('Ctrl Pts',(-0.433012701893303,0.424241377863696,
0.249999999998124));
#8215=CARTESIAN_POINT('Ctrl Pts',(-0.577350269189626,0.340908044531739,
-7.07050159149938E-17));
#8216=CARTESIAN_POINT('',(0.288675134594813,0.340908044531739,0.5));
#8217=CARTESIAN_POINT('Ctrl Pts',(0.288675134594813,0.340908044531739,0.5));
#8218=CARTESIAN_POINT('Ctrl Pts',(-2.16648921025353E-12,0.424241377863696,
0.5));
#8219=CARTESIAN_POINT('Ctrl Pts',(-0.288675134594813,0.340908044531739,
0.5));
#8220=CARTESIAN_POINT('',(0.577350269189626,0.340908044531739,0.));
#8221=CARTESIAN_POINT('Ctrl Pts',(0.577350269189626,0.340908044531739,0.));
#8222=CARTESIAN_POINT('Ctrl Pts',(0.433012701891136,0.424241377863697,0.250000000001876));
#8223=CARTESIAN_POINT('Ctrl Pts',(0.288675134594813,0.340908044531739,0.5));
#8224=CARTESIAN_POINT('',(0.288675134594813,0.340908044531739,-0.5));
#8225=CARTESIAN_POINT('Ctrl Pts',(0.288675134594813,0.340908044531739,-0.5));
#8226=CARTESIAN_POINT('Ctrl Pts',(0.433012701893303,0.424241377863696,-0.249999999998124));
#8227=CARTESIAN_POINT('Ctrl Pts',(0.577350269189626,0.340908044531739,0.));
#8228=CARTESIAN_POINT('',(-0.288675134594813,0.340908044531739,-0.5));
#8229=CARTESIAN_POINT('Ctrl Pts',(-0.288675134594813,0.340908044531739,
-0.5));
#8230=CARTESIAN_POINT('Ctrl Pts',(2.16660023255599E-12,0.424241377863696,
-0.5));
#8231=CARTESIAN_POINT('Ctrl Pts',(0.288675134594813,0.340908044531739,-0.5));
#8232=CARTESIAN_POINT('Ctrl Pts',(-0.577350269189626,0.340908044531739,
-7.07050159149938E-17));
#8233=CARTESIAN_POINT('Ctrl Pts',(-0.433012701891136,0.424241377863697,
-0.250000000001876));
#8234=CARTESIAN_POINT('Ctrl Pts',(-0.288675134594813,0.340908044531739,
-0.5));
#8235=CARTESIAN_POINT('Origin',(0.288675134594813,0.,-0.5));
#8236=CARTESIAN_POINT('',(0.288675134594813,0.,-0.5));
#8237=CARTESIAN_POINT('',(0.288675134594813,0.,-0.5));
#8238=CARTESIAN_POINT('',(-0.288675134594813,0.,-0.5));
#8239=CARTESIAN_POINT('',(0.288675134594813,0.,-0.5));
#8240=CARTESIAN_POINT('',(-0.288675134594813,0.,-0.5));
#8241=CARTESIAN_POINT('Origin',(0.577350269189626,0.,0.));
#8242=CARTESIAN_POINT('',(0.577350269189626,0.,0.));
#8243=CARTESIAN_POINT('',(0.577350269189626,0.,0.));
#8244=CARTESIAN_POINT('',(0.577350269189626,0.,0.));
#8245=CARTESIAN_POINT('Origin',(0.288675134594813,0.,0.5));
#8246=CARTESIAN_POINT('',(0.288675134594813,0.,0.5));
#8247=CARTESIAN_POINT('',(0.288675134594813,0.,0.5));
#8248=CARTESIAN_POINT('',(0.288675134594813,0.,0.5));
#8249=CARTESIAN_POINT('Origin',(-0.288675134594813,0.,0.5));
#8250=CARTESIAN_POINT('',(-0.288675134594813,0.,0.5));
#8251=CARTESIAN_POINT('',(-0.288675134594813,0.,0.5));
#8252=CARTESIAN_POINT('',(-0.288675134594813,0.,0.5));
#8253=CARTESIAN_POINT('Origin',(-0.577350269189626,0.,-7.07050159149938E-17));
#8254=CARTESIAN_POINT('',(-0.577350269189626,0.,-7.07050159149938E-17));
#8255=CARTESIAN_POINT('',(-0.577350269189626,0.,-7.07050159149938E-17));
#8256=CARTESIAN_POINT('',(-0.577350269189626,0.,-7.07050159149938E-17));
#8257=CARTESIAN_POINT('Origin',(-0.288675134594813,0.,-0.5));
#8258=CARTESIAN_POINT('',(-0.288675134594813,0.,-0.5));
#8259=CARTESIAN_POINT('Origin',(0.,0.4,0.));
#8260=CARTESIAN_POINT('Origin',(0.,0.,0.));
#9234=UNCERTAINTY_MEASURE_WITH_UNIT(LENGTH_MEASURE(0.001),#9286,
'DISTANCE_ACCURACY_VALUE',
'Maximum model space distance between geometric entities at asserted c
onnectivities');
#9255=UNCERTAINTY_MEASURE_WITH_UNIT(LENGTH_MEASURE(0.001),#9286,
'DISTANCE_ACCURACY_VALUE',
'Maximum model space distance between geometric entities at asserted c
onnectivities');
#9264=(
GEOMETRIC_REPRESENTATION_CONTEXT(3)
GLOBAL_UNCERTAINTY_ASSIGNED_CONTEXT((#9234))
GLOBAL_UNIT_ASSIGNED_CONTEXT((#9286,#9288,#9289))
REPRESENTATION_CONTEXT('','3D')
);
#9285=(
GEOMETRIC_REPRESENTATION_CONTEXT(3)
GLOBAL_UNCERTAINTY_ASSIGNED_CONTEXT((#9255))
GLOBAL_UNIT_ASSIGNED_CONTEXT((#9286,#9288,#9289))
REPRESENTATION_CONTEXT('','3D')
);
#9286=(
LENGTH_UNIT()
NAMED_UNIT(*)
SI_UNIT(.CENTI.,.METRE.)
);
#9288=(
NAMED_UNIT(*)
PLANE_ANGLE_UNIT()
SI_UNIT($,.RADIAN.)
);
#9289=(
NAMED_UNIT(*)
SI_UNIT($,.STERADIAN.)
SOLID_ANGLE_UNIT()
);
#9298=SHAPE_DEFINITION_REPRESENTATION(#9327,#9402);
#9327=PRODUCT_DEFINITION_SHAPE('',$,#9432);
#9402=SHAPE_REPRESENTATION('',(#5685),#9264);
#9423=PRODUCT_DEFINITION_CONTEXT('part definition',#9512,'design');
#9432=PRODUCT_DEFINITION('Hex Bolt - M6 x 30 mm',
'Hex Bolt - M6 x 30 mm',#9461,#9423);
#9461=PRODUCT_DEFINITION_FORMATION('',$,#9522);
#9512=APPLICATION_CONTEXT(
'Core Data for Automotive Mechanical Design Process');
#9513=PRODUCT_CONTEXT('part definition',#9512,'mechanical');
#9522=PRODUCT('Hex Bolt - M6 x 30 mm','Hex Bolt - M6 x 30 mm',
'Hex Bolt - M6 x 30 mm',(#9513));
#9613=COLOUR_RGB('Black',0.12,0.14,0.17);
#9614=FILL_AREA_STYLE_COLOUR('',#9613);
#9615=FILL_AREA_STYLE('',(#9614));
#9616=SURFACE_STYLE_FILL_AREA(#9615);
#9617=SURFACE_SIDE_STYLE('',(#9616));
#9618=SURFACE_STYLE_USAGE(.BOTH.,#9617);
#9619=PRESENTATION_STYLE_ASSIGNMENT((#9618));
ENDSEC;
END-ISO-10303-21;
